ISO-10303-21;
HEADER;
/* Generated by software containing ST-Developer
 * from STEP Tools, Inc. (www.steptools.com) 
 */

FILE_DESCRIPTION(
/* description */ ('PAT-080'),
/* implementation_level */ '2;1');

FILE_NAME(
/* name */ 'M5x14 Cap Screw.step',
/* time_stamp */ '2026-10-29T20:13:47-07:00',
/* author */ (''),
/* organization */ (''),
/* preprocessor_version */ 'ST-DEVELOPER v20.2',
/* originating_system */ 'Autodesk Translation Framework v15.17.0.0',
/* authorisation */ '');

FILE_SCHEMA (('AUTOMOTIVE_DESIGN { 1 0 10303 214 3 1 1 }'));
ENDSEC;

DATA;
#10=MECHANICAL_DESIGN_GEOMETRIC_PRESENTATION_REPRESENTATION('',(#258),#6878);
#187=CONICAL_SURFACE('',#4342,0.4,0.785398163397448);
#188=CONICAL_SURFACE('',#4346,0.41,0.785398163397448);
#189=CONICAL_SURFACE('',#4350,0.26,0.463647609000806);
#202=ORIENTED_CLOSED_SHELL('',*,#3874,.F.);
#205=BREP_WITH_VOIDS('Body1',#3875,(#202));
#220=SHAPE_REPRESENTATION_RELATIONSHIP('SRR','None',#6976,#239);
#239=ADVANCED_BREP_SHAPE_REPRESENTATION('',(#205),#6871);
#258=STYLED_ITEM('',(#7136),#205);
#339=FACE_BOUND('',#928,.T.);
#441=PLANE('',#4330);
#442=PLANE('',#4331);
#443=PLANE('',#4332);
#444=PLANE('',#4333);
#445=PLANE('',#4334);
#446=PLANE('',#4335);
#447=PLANE('',#4336);
#448=PLANE('',#4337);
#449=PLANE('',#4338);
#450=PLANE('',#4340);
#451=PLANE('',#4348);
#630=FACE_OUTER_BOUND('',#914,.T.);
#631=FACE_OUTER_BOUND('',#915,.T.);
#632=FACE_OUTER_BOUND('',#916,.T.);
#633=FACE_OUTER_BOUND('',#917,.T.);
#634=FACE_OUTER_BOUND('',#918,.T.);
#635=FACE_OUTER_BOUND('',#919,.T.);
#636=FACE_OUTER_BOUND('',#920,.T.);
#637=FACE_OUTER_BOUND('',#921,.T.);
#638=FACE_OUTER_BOUND('',#922,.T.);
#639=FACE_OUTER_BOUND('',#923,.T.);
#640=FACE_OUTER_BOUND('',#924,.T.);
#641=FACE_OUTER_BOUND('',#925,.T.);
#642=FACE_OUTER_BOUND('',#926,.T.);
#643=FACE_OUTER_BOUND('',#927,.T.);
#644=FACE_OUTER_BOUND('',#929,.T.);
#645=FACE_OUTER_BOUND('',#930,.T.);
#914=EDGE_LOOP('',(#3196,#3197,#3198,#3199));
#915=EDGE_LOOP('',(#3200,#3201,#3202,#3203));
#916=EDGE_LOOP('',(#3204,#3205,#3206,#3207));
#917=EDGE_LOOP('',(#3208,#3209,#3210,#3211));
#918=EDGE_LOOP('',(#3212,#3213,#3214,#3215));
#919=EDGE_LOOP('',(#3216,#3217,#3218,#3219));
#920=EDGE_LOOP('',(#3220,#3221,#3222,#3223,#3224,#3225));
#921=EDGE_LOOP('',(#3226,#3227,#3228,#3229,#3230,#3231));
#922=EDGE_LOOP('',(#3232));
#923=EDGE_LOOP('',(#3233));
#924=EDGE_LOOP('',(#3234,#3235,#3236,#3237));
#925=EDGE_LOOP('',(#3238,#3239,#3240,#3241));
#926=EDGE_LOOP('',(#3242,#3243,#3244,#3245));
#927=EDGE_LOOP('',(#3246));
#928=EDGE_LOOP('',(#3247));
#929=EDGE_LOOP('',(#3248,#3249,#3250,#3251));
#930=EDGE_LOOP('',(#3252,#3253,#3254,#3255));
#1230=LINE('',#6366,#1545);
#1231=LINE('',#6368,#1546);
#1232=LINE('',#6370,#1547);
#1233=LINE('',#6371,#1548);
#1234=LINE('',#6374,#1549);
#1235=LINE('',#6376,#1550);
#1236=LINE('',#6377,#1551);
#1237=LINE('',#6380,#1552);
#1238=LINE('',#6382,#1553);
#1239=LINE('',#6383,#1554);
#1240=LINE('',#6386,#1555);
#1241=LINE('',#6388,#1556);
#1242=LINE('',#6389,#1557);
#1243=LINE('',#6392,#1558);
#1244=LINE('',#6394,#1559);
#1245=LINE('',#6395,#1560);
#1246=LINE('',#6397,#1561);
#1247=LINE('',#6398,#1562);
#1248=LINE('',#6410,#1563);
#1249=LINE('',#6414,#1564);
#1250=LINE('',#6418,#1565);
#1251=LINE('',#6425,#1566);
#1252=LINE('',#6427,#1567);
#1545=VECTOR('',#5210,1.);
#1546=VECTOR('',#5211,1.);
#1547=VECTOR('',#5212,1.);
#1548=VECTOR('',#5213,1.);
#1549=VECTOR('',#5216,1.);
#1550=VECTOR('',#5217,1.);
#1551=VECTOR('',#5218,1.);
#1552=VECTOR('',#5221,1.);
#1553=VECTOR('',#5222,1.);
#1554=VECTOR('',#5223,1.);
#1555=VECTOR('',#5226,1.);
#1556=VECTOR('',#5227,1.);
#1557=VECTOR('',#5228,1.);
#1558=VECTOR('',#5231,1.);
#1559=VECTOR('',#5232,1.);
#1560=VECTOR('',#5233,1.);
#1561=VECTOR('',#5236,1.);
#1562=VECTOR('',#5237,1.);
#1563=VECTOR('',#5254,0.4);
#1564=VECTOR('',#5259,0.425);
#1565=VECTOR('',#5264,0.41);
#1566=VECTOR('',#5273,0.26);
#1567=VECTOR('',#5276,0.25);
#1750=CIRCLE('',#4339,0.24505);
#1751=CIRCLE('',#4341,0.375);
#1752=CIRCLE('',#4343,0.425);
#1753=CIRCLE('',#4345,0.425);
#1754=CIRCLE('',#4347,0.395);
#1755=CIRCLE('',#4349,0.27);
#1756=CIRCLE('',#4351,0.24505);
#2006=VERTEX_POINT('',#6364);
#2007=VERTEX_POINT('',#6365);
#2008=VERTEX_POINT('',#6367);
#2009=VERTEX_POINT('',#6369);
#2010=VERTEX_POINT('',#6373);
#2011=VERTEX_POINT('',#6375);
#2012=VERTEX_POINT('',#6379);
#2013=VERTEX_POINT('',#6381);
#2014=VERTEX_POINT('',#6385);
#2015=VERTEX_POINT('',#6387);
#2016=VERTEX_POINT('',#6391);
#2017=VERTEX_POINT('',#6393);
#2018=VERTEX_POINT('',#6402);
#2019=VERTEX_POINT('',#6405);
#2020=VERTEX_POINT('',#6408);
#2021=VERTEX_POINT('',#6412);
#2022=VERTEX_POINT('',#6416);
#2023=VERTEX_POINT('',#6420);
#2024=VERTEX_POINT('',#6423);
#2421=EDGE_CURVE('',#2006,#2007,#1230,.T.);
#2422=EDGE_CURVE('',#2007,#2008,#1231,.T.);
#2423=EDGE_CURVE('',#2008,#2009,#1232,.T.);
#2424=EDGE_CURVE('',#2006,#2009,#1233,.T.);
#2425=EDGE_CURVE('',#2007,#2010,#1234,.T.);
#2426=EDGE_CURVE('',#2010,#2011,#1235,.T.);
#2427=EDGE_CURVE('',#2011,#2008,#1236,.T.);
#2428=EDGE_CURVE('',#2010,#2012,#1237,.T.);
#2429=EDGE_CURVE('',#2012,#2013,#1238,.T.);
#2430=EDGE_CURVE('',#2013,#2011,#1239,.T.);
#2431=EDGE_CURVE('',#2012,#2014,#1240,.T.);
#2432=EDGE_CURVE('',#2014,#2015,#1241,.T.);
#2433=EDGE_CURVE('',#2015,#2013,#1242,.T.);
#2434=EDGE_CURVE('',#2014,#2016,#1243,.T.);
#2435=EDGE_CURVE('',#2016,#2017,#1244,.T.);
#2436=EDGE_CURVE('',#2017,#2015,#1245,.T.);
#2437=EDGE_CURVE('',#2016,#2006,#1246,.T.);
#2438=EDGE_CURVE('',#2009,#2017,#1247,.T.);
#2439=EDGE_CURVE('',#2018,#2018,#1750,.T.);
#2440=EDGE_CURVE('',#2019,#2019,#1751,.T.);
#2441=EDGE_CURVE('',#2020,#2020,#1752,.T.);
#2442=EDGE_CURVE('',#2020,#2019,#1248,.T.);
#2443=EDGE_CURVE('',#2021,#2021,#1753,.T.);
#2444=EDGE_CURVE('',#2021,#2020,#1249,.T.);
#2445=EDGE_CURVE('',#2022,#2022,#1754,.T.);
#2446=EDGE_CURVE('',#2022,#2021,#1250,.T.);
#2447=EDGE_CURVE('',#2023,#2023,#1755,.T.);
#2448=EDGE_CURVE('',#2024,#2024,#1756,.F.);
#2449=EDGE_CURVE('',#2024,#2023,#1251,.T.);
#2450=EDGE_CURVE('',#2018,#2024,#1252,.T.);
#3196=ORIENTED_EDGE('',*,*,#2421,.T.);
#3197=ORIENTED_EDGE('',*,*,#2422,.T.);
#3198=ORIENTED_EDGE('',*,*,#2423,.T.);
#3199=ORIENTED_EDGE('',*,*,#2424,.F.);
#3200=ORIENTED_EDGE('',*,*,#2425,.T.);
#3201=ORIENTED_EDGE('',*,*,#2426,.T.);
#3202=ORIENTED_EDGE('',*,*,#2427,.T.);
#3203=ORIENTED_EDGE('',*,*,#2422,.F.);
#3204=ORIENTED_EDGE('',*,*,#2428,.T.);
#3205=ORIENTED_EDGE('',*,*,#2429,.T.);
#3206=ORIENTED_EDGE('',*,*,#2430,.T.);
#3207=ORIENTED_EDGE('',*,*,#2426,.F.);
#3208=ORIENTED_EDGE('',*,*,#2431,.T.);
#3209=ORIENTED_EDGE('',*,*,#2432,.T.);
#3210=ORIENTED_EDGE('',*,*,#2433,.T.);
#3211=ORIENTED_EDGE('',*,*,#2429,.F.);
#3212=ORIENTED_EDGE('',*,*,#2434,.T.);
#3213=ORIENTED_EDGE('',*,*,#2435,.T.);
#3214=ORIENTED_EDGE('',*,*,#2436,.T.);
#3215=ORIENTED_EDGE('',*,*,#2432,.F.);
#3216=ORIENTED_EDGE('',*,*,#2437,.T.);
#3217=ORIENTED_EDGE('',*,*,#2424,.T.);
#3218=ORIENTED_EDGE('',*,*,#2438,.T.);
#3219=ORIENTED_EDGE('',*,*,#2435,.F.);
#3220=ORIENTED_EDGE('',*,*,#2437,.F.);
#3221=ORIENTED_EDGE('',*,*,#2434,.F.);
#3222=ORIENTED_EDGE('',*,*,#2431,.F.);
#3223=ORIENTED_EDGE('',*,*,#2428,.F.);
#3224=ORIENTED_EDGE('',*,*,#2425,.F.);
#3225=ORIENTED_EDGE('',*,*,#2421,.F.);
#3226=ORIENTED_EDGE('',*,*,#2438,.F.);
#3227=ORIENTED_EDGE('',*,*,#2423,.F.);
#3228=ORIENTED_EDGE('',*,*,#2427,.F.);
#3229=ORIENTED_EDGE('',*,*,#2430,.F.);
#3230=ORIENTED_EDGE('',*,*,#2433,.F.);
#3231=ORIENTED_EDGE('',*,*,#2436,.F.);
#3232=ORIENTED_EDGE('',*,*,#2439,.F.);
#3233=ORIENTED_EDGE('',*,*,#2440,.F.);
#3234=ORIENTED_EDGE('',*,*,#2441,.F.);
#3235=ORIENTED_EDGE('',*,*,#2442,.T.);
#3236=ORIENTED_EDGE('',*,*,#2440,.T.);
#3237=ORIENTED_EDGE('',*,*,#2442,.F.);
#3238=ORIENTED_EDGE('',*,*,#2443,.F.);
#3239=ORIENTED_EDGE('',*,*,#2444,.T.);
#3240=ORIENTED_EDGE('',*,*,#2441,.T.);
#3241=ORIENTED_EDGE('',*,*,#2444,.F.);
#3242=ORIENTED_EDGE('',*,*,#2445,.F.);
#3243=ORIENTED_EDGE('',*,*,#2446,.T.);
#3244=ORIENTED_EDGE('',*,*,#2443,.T.);
#3245=ORIENTED_EDGE('',*,*,#2446,.F.);
#3246=ORIENTED_EDGE('',*,*,#2445,.T.);
#3247=ORIENTED_EDGE('',*,*,#2447,.F.);
#3248=ORIENTED_EDGE('',*,*,#2448,.F.);
#3249=ORIENTED_EDGE('',*,*,#2449,.T.);
#3250=ORIENTED_EDGE('',*,*,#2447,.T.);
#3251=ORIENTED_EDGE('',*,*,#2449,.F.);
#3252=ORIENTED_EDGE('',*,*,#2439,.T.);
#3253=ORIENTED_EDGE('',*,*,#2450,.T.);
#3254=ORIENTED_EDGE('',*,*,#2448,.T.);
#3255=ORIENTED_EDGE('',*,*,#2450,.F.);
#3616=CYLINDRICAL_SURFACE('',#4344,0.425);
#3617=CYLINDRICAL_SURFACE('',#4352,0.24505);
#3766=ADVANCED_FACE('',(#630),#441,.F.);
#3767=ADVANCED_FACE('',(#631),#442,.F.);
#3768=ADVANCED_FACE('',(#632),#443,.F.);
#3769=ADVANCED_FACE('',(#633),#444,.F.);
#3770=ADVANCED_FACE('',(#634),#445,.F.);
#3771=ADVANCED_FACE('',(#635),#446,.F.);
#3772=ADVANCED_FACE('',(#636),#447,.F.);
#3773=ADVANCED_FACE('',(#637),#448,.F.);
#3774=ADVANCED_FACE('',(#638),#449,.F.);
#3775=ADVANCED_FACE('',(#639),#450,.T.);
#3776=ADVANCED_FACE('',(#640),#187,.T.);
#3777=ADVANCED_FACE('',(#641),#3616,.T.);
#3778=ADVANCED_FACE('',(#642),#188,.T.);
#3779=ADVANCED_FACE('',(#643,#339),#451,.T.);
#3780=ADVANCED_FACE('',(#644),#189,.T.);
#3781=ADVANCED_FACE('',(#645),#3617,.T.);
#3874=CLOSED_SHELL('',(#3766,#3767,#3768,#3769,#3770,#3771,#3772,#3773));
#3875=CLOSED_SHELL('',(#3774,#3775,#3776,#3777,#3778,#3779,#3780,#3781));
#4329=AXIS2_PLACEMENT_3D('',#6362,#5206,#5207);
#4330=AXIS2_PLACEMENT_3D('',#6363,#5208,#5209);
#4331=AXIS2_PLACEMENT_3D('',#6372,#5214,#5215);
#4332=AXIS2_PLACEMENT_3D('',#6378,#5219,#5220);
#4333=AXIS2_PLACEMENT_3D('',#6384,#5224,#5225);
#4334=AXIS2_PLACEMENT_3D('',#6390,#5229,#5230);
#4335=AXIS2_PLACEMENT_3D('',#6396,#5234,#5235);
#4336=AXIS2_PLACEMENT_3D('',#6399,#5238,#5239);
#4337=AXIS2_PLACEMENT_3D('',#6400,#5240,#5241);
#4338=AXIS2_PLACEMENT_3D('',#6401,#5242,#5243);
#4339=AXIS2_PLACEMENT_3D('',#6403,#5244,#5245);
#4340=AXIS2_PLACEMENT_3D('',#6404,#5246,#5247);
#4341=AXIS2_PLACEMENT_3D('',#6406,#5248,#5249);
#4342=AXIS2_PLACEMENT_3D('',#6407,#5250,#5251);
#4343=AXIS2_PLACEMENT_3D('',#6409,#5252,#5253);
#4344=AXIS2_PLACEMENT_3D('',#6411,#5255,#5256);
#4345=AXIS2_PLACEMENT_3D('',#6413,#5257,#5258);
#4346=AXIS2_PLACEMENT_3D('',#6415,#5260,#5261);
#4347=AXIS2_PLACEMENT_3D('',#6417,#5262,#5263);
#4348=AXIS2_PLACEMENT_3D('',#6419,#5265,#5266);
#4349=AXIS2_PLACEMENT_3D('',#6421,#5267,#5268);
#4350=AXIS2_PLACEMENT_3D('',#6422,#5269,#5270);
#4351=AXIS2_PLACEMENT_3D('',#6424,#5271,#5272);
#4352=AXIS2_PLACEMENT_3D('',#6426,#5274,#5275);
#5206=DIRECTION('axis',(0.,0.,1.));
#5207=DIRECTION('refdir',(1.,0.,0.));
#5208=DIRECTION('center_axis',(0.866025403784439,0.,-0.5));
#5209=DIRECTION('ref_axis',(0.5,0.,0.866025403784439));
#5210=DIRECTION('',(-0.5,0.,-0.866025403784439));
#5211=DIRECTION('',(0.,-1.,0.));
#5212=DIRECTION('',(0.5,0.,0.866025403784439));
#5213=DIRECTION('',(0.,-1.,0.));
#5214=DIRECTION('center_axis',(1.20185167898973E-16,0.,-1.));
#5215=DIRECTION('ref_axis',(1.,0.,1.20185167898973E-16));
#5216=DIRECTION('',(-1.,0.,-1.20185167898973E-16));
#5217=DIRECTION('',(0.,-1.,0.));
#5218=DIRECTION('',(1.,0.,1.20185167898973E-16));
#5219=DIRECTION('center_axis',(-0.866025403784439,0.,-0.5));
#5220=DIRECTION('ref_axis',(0.5,0.,-0.866025403784439));
#5221=DIRECTION('',(-0.5,0.,0.866025403784439));
#5222=DIRECTION('',(0.,-1.,0.));
#5223=DIRECTION('',(0.5,0.,-0.866025403784439));
#5224=DIRECTION('center_axis',(-0.866025403784439,0.,0.5));
#5225=DIRECTION('ref_axis',(-0.5,0.,-0.866025403784439));
#5226=DIRECTION('',(0.5,0.,0.866025403784439));
#5227=DIRECTION('',(0.,-1.,0.));
#5228=DIRECTION('',(-0.5,0.,-0.866025403784439));
#5229=DIRECTION('center_axis',(-2.40370335797945E-16,0.,1.));
#5230=DIRECTION('ref_axis',(-1.,0.,-2.40370335797945E-16));
#5231=DIRECTION('',(1.,0.,2.40370335797945E-16));
#5232=DIRECTION('',(0.,-1.,0.));
#5233=DIRECTION('',(-1.,0.,-2.40370335797945E-16));
#5234=DIRECTION('center_axis',(0.866025403784439,0.,0.5));
#5235=DIRECTION('ref_axis',(-0.5,0.,0.866025403784439));
#5236=DIRECTION('',(0.5,0.,-0.866025403784439));
#5237=DIRECTION('',(-0.5,0.,0.866025403784439));
#5238=DIRECTION('center_axis',(0.,1.,0.));
#5239=DIRECTION('ref_axis',(1.,0.,0.));
#5240=DIRECTION('center_axis',(0.,-1.,0.));
#5241=DIRECTION('ref_axis',(0.,0.,-1.));
#5242=DIRECTION('center_axis',(0.,1.,0.));
#5243=DIRECTION('ref_axis',(1.,0.,0.));
#5244=DIRECTION('center_axis',(0.,1.,0.));
#5245=DIRECTION('ref_axis',(1.,0.,0.));
#5246=DIRECTION('center_axis',(0.,1.,0.));
#5247=DIRECTION('ref_axis',(0.,0.,1.));
#5248=DIRECTION('center_axis',(0.,-1.,0.));
#5249=DIRECTION('ref_axis',(1.,0.,0.));
#5250=DIRECTION('center_axis',(0.,-1.,0.));
#5251=DIRECTION('ref_axis',(1.,0.,0.));
#5252=DIRECTION('center_axis',(0.,-1.,0.));
#5253=DIRECTION('ref_axis',(1.,0.,0.));
#5254=DIRECTION('',(0.707106781186548,0.707106781186547,8.65956056235493E-17));
#5255=DIRECTION('center_axis',(0.,-1.,0.));
#5256=DIRECTION('ref_axis',(1.,0.,0.));
#5257=DIRECTION('center_axis',(0.,-1.,0.));
#5258=DIRECTION('ref_axis',(1.,0.,0.));
#5259=DIRECTION('',(0.,1.,0.));
#5260=DIRECTION('center_axis',(0.,1.,0.));
#5261=DIRECTION('ref_axis',(1.,0.,0.));
#5262=DIRECTION('center_axis',(0.,-1.,0.));
#5263=DIRECTION('ref_axis',(1.,0.,0.));
#5264=DIRECTION('',(-0.707106781186547,0.707106781186548,-8.65956056235493E-17));
#5265=DIRECTION('center_axis',(0.,-1.,0.));
#5266=DIRECTION('ref_axis',(0.,0.,-1.));
#5267=DIRECTION('center_axis',(0.,-1.,0.));
#5268=DIRECTION('ref_axis',(1.,0.,0.));
#5269=DIRECTION('center_axis',(0.,1.,0.));
#5270=DIRECTION('ref_axis',(1.,0.,0.));
#5271=DIRECTION('center_axis',(0.,1.,0.));
#5272=DIRECTION('ref_axis',(1.,0.,0.));
#5273=DIRECTION('',(-0.447213595499958,0.894427190999916,-5.47678698264203E-17));
#5274=DIRECTION('center_axis',(0.,-1.,0.));
#5275=DIRECTION('ref_axis',(1.,0.,0.));
#5276=DIRECTION('',(0.,1.,0.));
#6362=CARTESIAN_POINT('',(0.,0.,0.));
#6363=CARTESIAN_POINT('Origin',(0.115470053837925,-0.5,-0.2));
#6364=CARTESIAN_POINT('',(0.23094010767585,-0.5,0.));
#6365=CARTESIAN_POINT('',(0.115470053837925,-0.5,-0.2));
#6366=CARTESIAN_POINT('',(0.23094010767585,-0.5,0.));
#6367=CARTESIAN_POINT('',(0.115470053837925,-0.8,-0.2));
#6368=CARTESIAN_POINT('',(0.115470053837925,-0.5,-0.2));
#6369=CARTESIAN_POINT('',(0.23094010767585,-0.8,0.));
#6370=CARTESIAN_POINT('',(0.23094010767585,-0.8,0.));
#6371=CARTESIAN_POINT('',(0.23094010767585,-0.5,0.));
#6372=CARTESIAN_POINT('Origin',(-0.115470053837925,-0.5,-0.2));
#6373=CARTESIAN_POINT('',(-0.115470053837925,-0.5,-0.2));
#6374=CARTESIAN_POINT('',(0.115470053837925,-0.5,-0.2));
#6375=CARTESIAN_POINT('',(-0.115470053837925,-0.8,-0.2));
#6376=CARTESIAN_POINT('',(-0.115470053837925,-0.5,-0.2));
#6377=CARTESIAN_POINT('',(0.115470053837925,-0.8,-0.2));
#6378=CARTESIAN_POINT('Origin',(-0.23094010767585,-0.5,-2.77555756156289E-17));
#6379=CARTESIAN_POINT('',(-0.23094010767585,-0.5,-2.82820063659975E-17));
#6380=CARTESIAN_POINT('',(-0.115470053837925,-0.5,-0.2));
#6381=CARTESIAN_POINT('',(-0.23094010767585,-0.8,-2.77555756156289E-17));
#6382=CARTESIAN_POINT('',(-0.23094010767585,-0.5,-2.82820063659975E-17));
#6383=CARTESIAN_POINT('',(-0.115470053837925,-0.8,-0.2));
#6384=CARTESIAN_POINT('Origin',(-0.115470053837925,-0.5,0.2));
#6385=CARTESIAN_POINT('',(-0.115470053837925,-0.5,0.2));
#6386=CARTESIAN_POINT('',(-0.23094010767585,-0.5,-2.82820063659975E-17));
#6387=CARTESIAN_POINT('',(-0.115470053837925,-0.8,0.2));
#6388=CARTESIAN_POINT('',(-0.115470053837925,-0.5,0.2));
#6389=CARTESIAN_POINT('',(-0.23094010767585,-0.8,-2.82820063659975E-17));
#6390=CARTESIAN_POINT('Origin',(0.115470053837925,-0.5,0.2));
#6391=CARTESIAN_POINT('',(0.115470053837925,-0.5,0.2));
#6392=CARTESIAN_POINT('',(-0.115470053837925,-0.5,0.2));
#6393=CARTESIAN_POINT('',(0.115470053837925,-0.8,0.2));
#6394=CARTESIAN_POINT('',(0.115470053837925,-0.5,0.2));
#6395=CARTESIAN_POINT('',(-0.115470053837925,-0.8,0.2));
#6396=CARTESIAN_POINT('Origin',(0.23094010767585,-0.5,0.));
#6397=CARTESIAN_POINT('',(0.115470053837925,-0.5,0.2));
#6398=CARTESIAN_POINT('',(0.115470053837925,-0.8,0.2));
#6399=CARTESIAN_POINT('Origin',(0.,-0.5,0.));
#6400=CARTESIAN_POINT('Origin',(0.,-0.8,0.));
#6401=CARTESIAN_POINT('Origin',(0.,-1.4,0.));
#6402=CARTESIAN_POINT('',(-0.24505,-1.4,3.00099698131059E-17));
#6403=CARTESIAN_POINT('Origin',(0.,-1.4,0.));
#6404=CARTESIAN_POINT('Origin',(0.375,0.5,0.));
#6405=CARTESIAN_POINT('',(-0.375,0.5,-4.59242549680257E-17));
#6406=CARTESIAN_POINT('Origin',(0.,0.5,0.));
#6407=CARTESIAN_POINT('Origin',(0.,0.475,0.));
#6408=CARTESIAN_POINT('',(-0.425,0.45,-5.20474889637625E-17));
#6409=CARTESIAN_POINT('Origin',(0.,0.45,0.));
#6410=CARTESIAN_POINT('',(-0.4,0.475,-4.89858719658941E-17));
#6411=CARTESIAN_POINT('Origin',(0.,0.24,0.));
#6412=CARTESIAN_POINT('',(-0.425,0.0299999999999998,-5.20474889637625E-17));
#6413=CARTESIAN_POINT('Origin',(0.,0.0299999999999998,0.));
#6414=CARTESIAN_POINT('',(-0.425,0.24,-5.20474889637625E-17));
#6415=CARTESIAN_POINT('Origin',(0.,0.0150000000000001,0.));
#6416=CARTESIAN_POINT('',(-0.395,4.85722573273506E-17,-4.83735485663204E-17));
#6417=CARTESIAN_POINT('Origin',(0.,0.,0.));
#6418=CARTESIAN_POINT('',(-0.41,0.0150000000000001,-5.02105187650415E-17));
#6419=CARTESIAN_POINT('Origin',(0.27,0.,0.));
#6420=CARTESIAN_POINT('',(-0.27,0.,-3.30654635769785E-17));
#6421=CARTESIAN_POINT('Origin',(0.,0.,0.));
#6422=CARTESIAN_POINT('Origin',(0.,-0.02,0.));
#6423=CARTESIAN_POINT('',(-0.24505,-0.0498999999999999,3.00099698131059E-17));
#6424=CARTESIAN_POINT('Origin',(0.,-0.0498999999999999,0.));
#6425=CARTESIAN_POINT('',(-0.26,-0.02,-3.18408167778312E-17));
#6426=CARTESIAN_POINT('Origin',(0.,-0.995,0.));
#6427=CARTESIAN_POINT('',(-0.24505,-0.995,-3.00099698131059E-17));
#6850=UNCERTAINTY_MEASURE_WITH_UNIT(LENGTH_MEASURE(0.001),#6879,
'DISTANCE_ACCURACY_VALUE',
'Maximum model space distance between geometric entities at asserted c
onnectivities');
#6857=UNCERTAINTY_MEASURE_WITH_UNIT(LENGTH_MEASURE(0.001),#6879,
'DISTANCE_ACCURACY_VALUE',
'Maximum model space distance between geometric entities at asserted c
onnectivities');
#6871=(
GEOMETRIC_REPRESENTATION_CONTEXT(3)
GLOBAL_UNCERTAINTY_ASSIGNED_CONTEXT((#6850))
GLOBAL_UNIT_ASSIGNED_CONTEXT((#6879,#6881,#6882))
REPRESENTATION_CONTEXT('','3D')
);
#6878=(
GEOMETRIC_REPRESENTATION_CONTEXT(3)
GLOBAL_UNCERTAINTY_ASSIGNED_CONTEXT((#6857))
GLOBAL_UNIT_ASSIGNED_CONTEXT((#6879,#6881,#6882))
REPRESENTATION_CONTEXT('','3D')
);
#6879=(
LENGTH_UNIT()
NAMED_UNIT(*)
SI_UNIT(.CENTI.,.METRE.)
);
#6881=(
NAMED_UNIT(*)
PLANE_ANGLE_UNIT()
SI_UNIT($,.RADIAN.)
);
#6882=(
NAMED_UNIT(*)
SI_UNIT($,.STERADIAN.)
SOLID_ANGLE_UNIT()
);
#6896=SHAPE_DEFINITION_REPRESENTATION(#6916,#6976);
#6916=PRODUCT_DEFINITION_SHAPE('',$,#6997);
#6976=SHAPE_REPRESENTATION('',(#4329),#6871);
#6983=PRODUCT_DEFINITION_CONTEXT('part definition',#7045,'design');
#6997=PRODUCT_DEFINITION('M5x14 Cap Screw','M5x14 Cap Screw',
#7017,#6983);
#7017=PRODUCT_DEFINITION_FORMATION('',$,#7060);
#7045=APPLICATION_CONTEXT(
'Core Data for Automotive Mechanical Design Process');
#7046=PRODUCT_CONTEXT('part definition',#7045,'mechanical');
#7060=PRODUCT('M5x14 Cap Screw','M5x14 Cap Screw',
'M5x14 Cap Screw',(#7046));
#7130=COLOUR_RGB('Black',0.12,0.14,0.17);
#7131=FILL_AREA_STYLE_COLOUR('',#7130);
#7132=FILL_AREA_STYLE('',(#7131));
#7133=SURFACE_STYLE_FILL_AREA(#7132);
#7134=SURFACE_SIDE_STYLE('',(#7133));
#7135=SURFACE_STYLE_USAGE(.BOTH.,#7134);
#7136=PRESENTATION_STYLE_ASSIGNMENT((#7135));
ENDSEC;
END-ISO-10303-21;
